ISO-10303-21;
HEADER;
/* Generated by software containing ST-Developer
 * from STEP Tools, Inc. (www.steptools.com) 
 */

FILE_DESCRIPTION(
/* description */ ('Bin tilter linkage'),
/* implementation_level */ '2;1');

FILE_NAME(
/* name */ 'Screw keeper fastener (4).step',
/* time_stamp */ '2026-10-28T03:26:24-07:00',
/* author */ (''),
/* organization */ (''),
/* preprocessor_version */ 'ST-DEVELOPER v20.2',
/* originating_system */ 'Autodesk Translation Framework v15.17.0.0',
/* authorisation */ '');

FILE_SCHEMA (('AUTOMOTIVE_DESIGN { 1 0 10303 214 3 1 1 }'));
ENDSEC;

DATA;
#10=MECHANICAL_DESIGN_GEOMETRIC_PRESENTATION_REPRESENTATION('',(#884),#23728);
#672=SHAPE_REPRESENTATION_RELATIONSHIP('SRR','None',#24136,#778);
#778=ADVANCED_BREP_SHAPE_REPRESENTATION('',(#998),#23636);
#884=STYLED_ITEM('',(#24772),#998);
#998=MANIFOLD_SOLID_BREP('Body1',#12414);
#1223=FACE_BOUND('',#3001,.T.);
#1588=PLANE('',#14100);
#1589=PLANE('',#14105);
#1590=PLANE('',#14108);
#2087=FACE_OUTER_BOUND('',#3000,.T.);
#2088=FACE_OUTER_BOUND('',#3002,.T.);
#2089=FACE_OUTER_BOUND('',#3003,.T.);
#2090=FACE_OUTER_BOUND('',#3004,.T.);
#2091=FACE_OUTER_BOUND('',#3005,.T.);
#3000=EDGE_LOOP('',(#9207));
#3001=EDGE_LOOP('',(#9208));
#3002=EDGE_LOOP('',(#9209,#9210,#9211,#9212));
#3003=EDGE_LOOP('',(#9213));
#3004=EDGE_LOOP('',(#9214,#9215,#9216,#9217));
#3005=EDGE_LOOP('',(#9218));
#4064=LINE('',#20669,#4739);
#4065=LINE('',#20675,#4740);
#4739=VECTOR('',#16545,0.35);
#4740=VECTOR('',#16554,0.199999999999999);
#5401=CIRCLE('',#14101,0.35);
#5402=CIRCLE('',#14102,0.199999999999999);
#5403=CIRCLE('',#14104,0.35);
#5404=CIRCLE('',#14107,0.199999999999999);
#6235=VERTEX_POINT('',#20663);
#6236=VERTEX_POINT('',#20665);
#6237=VERTEX_POINT('',#20668);
#6238=VERTEX_POINT('',#20673);
#7343=EDGE_CURVE('',#6235,#6235,#5401,.T.);
#7344=EDGE_CURVE('',#6236,#6236,#5402,.T.);
#7345=EDGE_CURVE('',#6235,#6237,#4064,.T.);
#7346=EDGE_CURVE('',#6237,#6237,#5403,.T.);
#7347=EDGE_CURVE('',#6238,#6238,#5404,.T.);
#7348=EDGE_CURVE('',#6238,#6236,#4065,.T.);
#9207=ORIENTED_EDGE('',*,*,#7343,.T.);
#9208=ORIENTED_EDGE('',*,*,#7344,.F.);
#9209=ORIENTED_EDGE('',*,*,#7343,.F.);
#9210=ORIENTED_EDGE('',*,*,#7345,.T.);
#9211=ORIENTED_EDGE('',*,*,#7346,.T.);
#9212=ORIENTED_EDGE('',*,*,#7345,.F.);
#9213=ORIENTED_EDGE('',*,*,#7346,.F.);
#9214=ORIENTED_EDGE('',*,*,#7347,.F.);
#9215=ORIENTED_EDGE('',*,*,#7348,.T.);
#9216=ORIENTED_EDGE('',*,*,#7344,.T.);
#9217=ORIENTED_EDGE('',*,*,#7348,.F.);
#9218=ORIENTED_EDGE('',*,*,#7347,.T.);
#11368=CYLINDRICAL_SURFACE('',#14103,0.35);
#11369=CYLINDRICAL_SURFACE('',#14106,0.199999999999999);
#11812=ADVANCED_FACE('',(#2087,#1223),#1588,.T.);
#11813=ADVANCED_FACE('',(#2088),#11368,.T.);
#11814=ADVANCED_FACE('',(#2089),#1589,.F.);
#11815=ADVANCED_FACE('',(#2090),#11369,.T.);
#11816=ADVANCED_FACE('',(#2091),#1590,.T.);
#12414=CLOSED_SHELL('',(#11812,#11813,#11814,#11815,#11816));
#14099=AXIS2_PLACEMENT_3D('',#20661,#16535,#16536);
#14100=AXIS2_PLACEMENT_3D('',#20662,#16537,#16538);
#14101=AXIS2_PLACEMENT_3D('',#20664,#16539,#16540);
#14102=AXIS2_PLACEMENT_3D('',#20666,#16541,#16542);
#14103=AXIS2_PLACEMENT_3D('',#20667,#16543,#16544);
#14104=AXIS2_PLACEMENT_3D('',#20670,#16546,#16547);
#14105=AXIS2_PLACEMENT_3D('',#20671,#16548,#16549);
#14106=AXIS2_PLACEMENT_3D('',#20672,#16550,#16551);
#14107=AXIS2_PLACEMENT_3D('',#20674,#16552,#16553);
#14108=AXIS2_PLACEMENT_3D('',#20676,#16555,#16556);
#16535=DIRECTION('axis',(0.,0.,1.));
#16536=DIRECTION('refdir',(1.,0.,0.));
#16537=DIRECTION('center_axis',(1.,0.,0.));
#16538=DIRECTION('ref_axis',(0.,0.,-1.));
#16539=DIRECTION('center_axis',(1.,0.,0.));
#16540=DIRECTION('ref_axis',(0.,0.,-1.));
#16541=DIRECTION('center_axis',(1.,0.,0.));
#16542=DIRECTION('ref_axis',(0.,0.,-1.));
#16543=DIRECTION('center_axis',(1.,0.,0.));
#16544=DIRECTION('ref_axis',(0.,0.,-1.));
#16545=DIRECTION('',(-1.,0.,0.));
#16546=DIRECTION('center_axis',(1.,0.,0.));
#16547=DIRECTION('ref_axis',(0.,0.,-1.));
#16548=DIRECTION('center_axis',(1.,0.,0.));
#16549=DIRECTION('ref_axis',(0.,0.,-1.));
#16550=DIRECTION('center_axis',(1.,0.,0.));
#16551=DIRECTION('ref_axis',(0.,0.,-1.));
#16552=DIRECTION('center_axis',(1.,0.,0.));
#16553=DIRECTION('ref_axis',(0.,0.,-1.));
#16554=DIRECTION('',(-1.,0.,0.));
#16555=DIRECTION('center_axis',(1.,0.,0.));
#16556=DIRECTION('ref_axis',(0.,0.,-1.));
#20661=CARTESIAN_POINT('',(0.,0.,0.));
#20662=CARTESIAN_POINT('Origin',(-0.2,-4.5,9.85));
#20663=CARTESIAN_POINT('',(-0.2,-4.5,10.2));
#20664=CARTESIAN_POINT('Origin',(-0.2,-4.5,9.85));
#20665=CARTESIAN_POINT('',(-0.2,-4.5,10.05));
#20666=CARTESIAN_POINT('Origin',(-0.2,-4.5,9.85));
#20667=CARTESIAN_POINT('Origin',(-0.6,-4.5,9.85));
#20668=CARTESIAN_POINT('',(-0.6,-4.5,10.2));
#20669=CARTESIAN_POINT('',(-0.6,-4.5,10.2));
#20670=CARTESIAN_POINT('Origin',(-0.6,-4.5,9.85));
#20671=CARTESIAN_POINT('Origin',(-0.6,-4.5,9.85));
#20672=CARTESIAN_POINT('Origin',(-0.2,-4.5,9.85));
#20673=CARTESIAN_POINT('',(0.5,-4.5,10.05));
#20674=CARTESIAN_POINT('Origin',(0.5,-4.5,9.85));
#20675=CARTESIAN_POINT('',(-0.2,-4.5,10.05));
#20676=CARTESIAN_POINT('Origin',(0.5,-4.5,9.85));
#23519=UNCERTAINTY_MEASURE_WITH_UNIT(LENGTH_MEASURE(0.001),#23729,
'DISTANCE_ACCURACY_VALUE',
'Maximum model space distance between geometric entities at asserted c
onnectivities');
#23611=UNCERTAINTY_MEASURE_WITH_UNIT(LENGTH_MEASURE(0.001),#23729,
'DISTANCE_ACCURACY_VALUE',
'Maximum model space distance between geometric entities at asserted c
onnectivities');
#23636=(
GEOMETRIC_REPRESENTATION_CONTEXT(3)
GLOBAL_UNCERTAINTY_ASSIGNED_CONTEXT((#23519))
GLOBAL_UNIT_ASSIGNED_CONTEXT((#23729,#23731,#23732))
REPRESENTATION_CONTEXT('','3D')
);
#23728=(
GEOMETRIC_REPRESENTATION_CONTEXT(3)
GLOBAL_UNCERTAINTY_ASSIGNED_CONTEXT((#23611))
GLOBAL_UNIT_ASSIGNED_CONTEXT((#23729,#23731,#23732))
REPRESENTATION_CONTEXT('','3D')
);
#23729=(
LENGTH_UNIT()
NAMED_UNIT(*)
SI_UNIT(.CENTI.,.METRE.)
);
#23731=(
NAMED_UNIT(*)
PLANE_ANGLE_UNIT()
SI_UNIT($,.RADIAN.)
);
#23732=(
NAMED_UNIT(*)
SI_UNIT($,.STERADIAN.)
SOLID_ANGLE_UNIT()
);
#23757=SHAPE_DEFINITION_REPRESENTATION(#23873,#24136);
#23873=PRODUCT_DEFINITION_SHAPE('',$,#24253);
#24136=SHAPE_REPRESENTATION('',(#14099),#23636);
#24228=PRODUCT_DEFINITION_CONTEXT('part definition',#24578,'design');
#24253=PRODUCT_DEFINITION('Screw keeper fastener (4)',
'Screw keeper fastener (4)',#24369,#24228);
#24369=PRODUCT_DEFINITION_FORMATION('',$,#24604);
#24578=APPLICATION_CONTEXT(
'Core Data for Automotive Mechanical Design Process');
#24579=PRODUCT_CONTEXT('part definition',#24578,'mechanical');
#24604=PRODUCT('Screw keeper fastener (4)','Screw keeper fastener (4)',
'Screw keeper fastener (4)',(#24579));
#24766=COLOUR_RGB('Black',0.12,0.14,0.17);
#24767=FILL_AREA_STYLE_COLOUR('',#24766);
#24768=FILL_AREA_STYLE('',(#24767));
#24769=SURFACE_STYLE_FILL_AREA(#24768);
#24770=SURFACE_SIDE_STYLE('',(#24769));
#24771=SURFACE_STYLE_USAGE(.BOTH.,#24770);
#24772=PRESENTATION_STYLE_ASSIGNMENT((#24771));
ENDSEC;
END-ISO-10303-21;
